ISO-10303-21;
HEADER;
/* Generated by software containing ST-Developer
 * from STEP Tools, Inc. (www.steptools.com) 
 */

FILE_DESCRIPTION(
/* description */ ('PAT-080'),
/* implementation_level */ '2;1');

FILE_NAME(
/* name */ 'Union half B.step',
/* time_stamp */ '2026-10-29T20:13:47-07:00',
/* author */ (''),
/* organization */ (''),
/* preprocessor_version */ 'ST-DEVELOPER v20.2',
/* originating_system */ 'Autodesk Translation Framework v15.17.0.0',
/* authorisation */ '');

FILE_SCHEMA (('AUTOMOTIVE_DESIGN { 1 0 10303 214 3 1 1 }'));
ENDSEC;

DATA;
#10=MECHANICAL_DESIGN_GEOMETRIC_PRESENTATION_REPRESENTATION('',(#256),#6878);
#218=SHAPE_REPRESENTATION_RELATIONSHIP('SRR','None',#6974,#237);
#237=ADVANCED_BREP_SHAPE_REPRESENTATION('',(#275),#6869);
#256=STYLED_ITEM('',(#7122),#275);
#275=MANIFOLD_SOLID_BREP('Body1',#3872);
#326=FACE_BOUND('',#892,.T.);
#327=FACE_BOUND('',#893,.T.);
#328=FACE_BOUND('',#894,.T.);
#329=FACE_BOUND('',#895,.T.);
#330=FACE_BOUND('',#896,.T.);
#331=FACE_BOUND('',#901,.T.);
#332=FACE_BOUND('',#903,.T.);
#333=FACE_BOUND('',#904,.T.);
#334=FACE_BOUND('',#905,.T.);
#335=FACE_BOUND('',#906,.T.);
#336=FACE_BOUND('',#907,.T.);
#436=PLANE('',#4308);
#437=PLANE('',#4318);
#438=PLANE('',#4319);
#616=FACE_OUTER_BOUND('',#887,.T.);
#617=FACE_OUTER_BOUND('',#888,.T.);
#618=FACE_OUTER_BOUND('',#889,.T.);
#619=FACE_OUTER_BOUND('',#890,.T.);
#620=FACE_OUTER_BOUND('',#891,.T.);
#621=FACE_OUTER_BOUND('',#897,.T.);
#622=FACE_OUTER_BOUND('',#898,.T.);
#623=FACE_OUTER_BOUND('',#899,.T.);
#624=FACE_OUTER_BOUND('',#900,.T.);
#625=FACE_OUTER_BOUND('',#902,.T.);
#887=EDGE_LOOP('',(#3142,#3143,#3144,#3145));
#888=EDGE_LOOP('',(#3146,#3147,#3148,#3149));
#889=EDGE_LOOP('',(#3150,#3151,#3152,#3153));
#890=EDGE_LOOP('',(#3154,#3155,#3156,#3157));
#891=EDGE_LOOP('',(#3158));
#892=EDGE_LOOP('',(#3159));
#893=EDGE_LOOP('',(#3160));
#894=EDGE_LOOP('',(#3161));
#895=EDGE_LOOP('',(#3162));
#896=EDGE_LOOP('',(#3163));
#897=EDGE_LOOP('',(#3164,#3165,#3166,#3167));
#898=EDGE_LOOP('',(#3168,#3169,#3170,#3171));
#899=EDGE_LOOP('',(#3172,#3173,#3174,#3175));
#900=EDGE_LOOP('',(#3176));
#901=EDGE_LOOP('',(#3177));
#902=EDGE_LOOP('',(#3178));
#903=EDGE_LOOP('',(#3179));
#904=EDGE_LOOP('',(#3180));
#905=EDGE_LOOP('',(#3181));
#906=EDGE_LOOP('',(#3182));
#907=EDGE_LOOP('',(#3183));
#1221=LINE('',#6306,#1536);
#1222=LINE('',#6312,#1537);
#1223=LINE('',#6318,#1538);
#1224=LINE('',#6324,#1539);
#1225=LINE('',#6333,#1540);
#1226=LINE('',#6339,#1541);
#1227=LINE('',#6344,#1542);
#1536=VECTOR('',#5135,0.44);
#1537=VECTOR('',#5142,0.44);
#1538=VECTOR('',#5149,0.44);
#1539=VECTOR('',#5156,0.44);
#1540=VECTOR('',#5167,3.5);
#1541=VECTOR('',#5174,0.79);
#1542=VECTOR('',#5181,1.5);
#1732=CIRCLE('',#4297,0.44);
#1733=CIRCLE('',#4298,0.44);
#1734=CIRCLE('',#4300,0.44);
#1735=CIRCLE('',#4301,0.44);
#1736=CIRCLE('',#4303,0.44);
#1737=CIRCLE('',#4304,0.44);
#1738=CIRCLE('',#4306,0.44);
#1739=CIRCLE('',#4307,0.44);
#1740=CIRCLE('',#4309,3.5);
#1741=CIRCLE('',#4310,1.5);
#1742=CIRCLE('',#4312,3.5);
#1743=CIRCLE('',#4314,0.79);
#1744=CIRCLE('',#4315,0.79);
#1745=CIRCLE('',#4317,1.5);
#1988=VERTEX_POINT('',#6303);
#1989=VERTEX_POINT('',#6305);
#1990=VERTEX_POINT('',#6309);
#1991=VERTEX_POINT('',#6311);
#1992=VERTEX_POINT('',#6315);
#1993=VERTEX_POINT('',#6317);
#1994=VERTEX_POINT('',#6321);
#1995=VERTEX_POINT('',#6323);
#1996=VERTEX_POINT('',#6327);
#1997=VERTEX_POINT('',#6329);
#1998=VERTEX_POINT('',#6332);
#1999=VERTEX_POINT('',#6336);
#2000=VERTEX_POINT('',#6338);
#2001=VERTEX_POINT('',#6342);
#2394=EDGE_CURVE('',#1988,#1988,#1732,.T.);
#2395=EDGE_CURVE('',#1988,#1989,#1221,.T.);
#2396=EDGE_CURVE('',#1989,#1989,#1733,.T.);
#2397=EDGE_CURVE('',#1990,#1990,#1734,.T.);
#2398=EDGE_CURVE('',#1990,#1991,#1222,.T.);
#2399=EDGE_CURVE('',#1991,#1991,#1735,.T.);
#2400=EDGE_CURVE('',#1992,#1992,#1736,.T.);
#2401=EDGE_CURVE('',#1992,#1993,#1223,.T.);
#2402=EDGE_CURVE('',#1993,#1993,#1737,.T.);
#2403=EDGE_CURVE('',#1994,#1994,#1738,.T.);
#2404=EDGE_CURVE('',#1994,#1995,#1224,.T.);
#2405=EDGE_CURVE('',#1995,#1995,#1739,.T.);
#2406=EDGE_CURVE('',#1996,#1996,#1740,.T.);
#2407=EDGE_CURVE('',#1997,#1997,#1741,.T.);
#2408=EDGE_CURVE('',#1996,#1998,#1225,.T.);
#2409=EDGE_CURVE('',#1998,#1998,#1742,.T.);
#2410=EDGE_CURVE('',#1999,#1999,#1743,.T.);
#2411=EDGE_CURVE('',#1999,#2000,#1226,.T.);
#2412=EDGE_CURVE('',#2000,#2000,#1744,.T.);
#2413=EDGE_CURVE('',#2001,#2001,#1745,.T.);
#2414=EDGE_CURVE('',#2001,#1997,#1227,.T.);
#3142=ORIENTED_EDGE('',*,*,#2394,.F.);
#3143=ORIENTED_EDGE('',*,*,#2395,.T.);
#3144=ORIENTED_EDGE('',*,*,#2396,.F.);
#3145=ORIENTED_EDGE('',*,*,#2395,.F.);
#3146=ORIENTED_EDGE('',*,*,#2397,.F.);
#3147=ORIENTED_EDGE('',*,*,#2398,.T.);
#3148=ORIENTED_EDGE('',*,*,#2399,.F.);
#3149=ORIENTED_EDGE('',*,*,#2398,.F.);
#3150=ORIENTED_EDGE('',*,*,#2400,.F.);
#3151=ORIENTED_EDGE('',*,*,#2401,.T.);
#3152=ORIENTED_EDGE('',*,*,#2402,.F.);
#3153=ORIENTED_EDGE('',*,*,#2401,.F.);
#3154=ORIENTED_EDGE('',*,*,#2403,.F.);
#3155=ORIENTED_EDGE('',*,*,#2404,.T.);
#3156=ORIENTED_EDGE('',*,*,#2405,.F.);
#3157=ORIENTED_EDGE('',*,*,#2404,.F.);
#3158=ORIENTED_EDGE('',*,*,#2406,.T.);
#3159=ORIENTED_EDGE('',*,*,#2407,.F.);
#3160=ORIENTED_EDGE('',*,*,#2405,.T.);
#3161=ORIENTED_EDGE('',*,*,#2402,.T.);
#3162=ORIENTED_EDGE('',*,*,#2399,.T.);
#3163=ORIENTED_EDGE('',*,*,#2396,.T.);
#3164=ORIENTED_EDGE('',*,*,#2406,.F.);
#3165=ORIENTED_EDGE('',*,*,#2408,.T.);
#3166=ORIENTED_EDGE('',*,*,#2409,.T.);
#3167=ORIENTED_EDGE('',*,*,#2408,.F.);
#3168=ORIENTED_EDGE('',*,*,#2410,.F.);
#3169=ORIENTED_EDGE('',*,*,#2411,.T.);
#3170=ORIENTED_EDGE('',*,*,#2412,.T.);
#3171=ORIENTED_EDGE('',*,*,#2411,.F.);
#3172=ORIENTED_EDGE('',*,*,#2413,.F.);
#3173=ORIENTED_EDGE('',*,*,#2414,.T.);
#3174=ORIENTED_EDGE('',*,*,#2407,.T.);
#3175=ORIENTED_EDGE('',*,*,#2414,.F.);
#3176=ORIENTED_EDGE('',*,*,#2413,.T.);
#3177=ORIENTED_EDGE('',*,*,#2410,.T.);
#3178=ORIENTED_EDGE('',*,*,#2409,.F.);
#3179=ORIENTED_EDGE('',*,*,#2412,.F.);
#3180=ORIENTED_EDGE('',*,*,#2403,.T.);
#3181=ORIENTED_EDGE('',*,*,#2400,.T.);
#3182=ORIENTED_EDGE('',*,*,#2397,.T.);
#3183=ORIENTED_EDGE('',*,*,#2394,.T.);
#3607=CYLINDRICAL_SURFACE('',#4296,0.44);
#3608=CYLINDRICAL_SURFACE('',#4299,0.44);
#3609=CYLINDRICAL_SURFACE('',#4302,0.44);
#3610=CYLINDRICAL_SURFACE('',#4305,0.44);
#3611=CYLINDRICAL_SURFACE('',#4311,3.5);
#3612=CYLINDRICAL_SURFACE('',#4313,0.79);
#3613=CYLINDRICAL_SURFACE('',#4316,1.5);
#3752=ADVANCED_FACE('',(#616),#3607,.F.);
#3753=ADVANCED_FACE('',(#617),#3608,.F.);
#3754=ADVANCED_FACE('',(#618),#3609,.F.);
#3755=ADVANCED_FACE('',(#619),#3610,.F.);
#3756=ADVANCED_FACE('',(#620,#326,#327,#328,#329,#330),#436,.T.);
#3757=ADVANCED_FACE('',(#621),#3611,.T.);
#3758=ADVANCED_FACE('',(#622),#3612,.F.);
#3759=ADVANCED_FACE('',(#623),#3613,.T.);
#3760=ADVANCED_FACE('',(#624,#331),#437,.T.);
#3761=ADVANCED_FACE('',(#625,#332,#333,#334,#335,#336),#438,.F.);
#3872=CLOSED_SHELL('',(#3752,#3753,#3754,#3755,#3756,#3757,#3758,#3759,
#3760,#3761));
#4295=AXIS2_PLACEMENT_3D('',#6301,#5129,#5130);
#4296=AXIS2_PLACEMENT_3D('',#6302,#5131,#5132);
#4297=AXIS2_PLACEMENT_3D('',#6304,#5133,#5134);
#4298=AXIS2_PLACEMENT_3D('',#6307,#5136,#5137);
#4299=AXIS2_PLACEMENT_3D('',#6308,#5138,#5139);
#4300=AXIS2_PLACEMENT_3D('',#6310,#5140,#5141);
#4301=AXIS2_PLACEMENT_3D('',#6313,#5143,#5144);
#4302=AXIS2_PLACEMENT_3D('',#6314,#5145,#5146);
#4303=AXIS2_PLACEMENT_3D('',#6316,#5147,#5148);
#4304=AXIS2_PLACEMENT_3D('',#6319,#5150,#5151);
#4305=AXIS2_PLACEMENT_3D('',#6320,#5152,#5153);
#4306=AXIS2_PLACEMENT_3D('',#6322,#5154,#5155);
#4307=AXIS2_PLACEMENT_3D('',#6325,#5157,#5158);
#4308=AXIS2_PLACEMENT_3D('',#6326,#5159,#5160);
#4309=AXIS2_PLACEMENT_3D('',#6328,#5161,#5162);
#4310=AXIS2_PLACEMENT_3D('',#6330,#5163,#5164);
#4311=AXIS2_PLACEMENT_3D('',#6331,#5165,#5166);
#4312=AXIS2_PLACEMENT_3D('',#6334,#5168,#5169);
#4313=AXIS2_PLACEMENT_3D('',#6335,#5170,#5171);
#4314=AXIS2_PLACEMENT_3D('',#6337,#5172,#5173);
#4315=AXIS2_PLACEMENT_3D('',#6340,#5175,#5176);
#4316=AXIS2_PLACEMENT_3D('',#6341,#5177,#5178);
#4317=AXIS2_PLACEMENT_3D('',#6343,#5179,#5180);
#4318=AXIS2_PLACEMENT_3D('',#6345,#5182,#5183);
#4319=AXIS2_PLACEMENT_3D('',#6346,#5184,#5185);
#5129=DIRECTION('axis',(0.,0.,1.));
#5130=DIRECTION('refdir',(1.,0.,0.));
#5131=DIRECTION('center_axis',(1.,0.,0.));
#5132=DIRECTION('ref_axis',(0.,0.,-1.));
#5133=DIRECTION('center_axis',(1.,0.,0.));
#5134=DIRECTION('ref_axis',(0.,0.,-1.));
#5135=DIRECTION('',(1.,0.,0.));
#5136=DIRECTION('center_axis',(-1.,0.,0.));
#5137=DIRECTION('ref_axis',(0.,0.,-1.));
#5138=DIRECTION('center_axis',(1.,0.,0.));
#5139=DIRECTION('ref_axis',(0.,0.,-1.));
#5140=DIRECTION('center_axis',(1.,0.,0.));
#5141=DIRECTION('ref_axis',(0.,0.,-1.));
#5142=DIRECTION('',(1.,0.,0.));
#5143=DIRECTION('center_axis',(-1.,0.,0.));
#5144=DIRECTION('ref_axis',(0.,0.,-1.));
#5145=DIRECTION('center_axis',(1.,0.,0.));
#5146=DIRECTION('ref_axis',(0.,0.,-1.));
#5147=DIRECTION('center_axis',(1.,0.,0.));
#5148=DIRECTION('ref_axis',(0.,0.,-1.));
#5149=DIRECTION('',(1.,0.,0.));
#5150=DIRECTION('center_axis',(-1.,0.,0.));
#5151=DIRECTION('ref_axis',(0.,0.,-1.));
#5152=DIRECTION('center_axis',(1.,0.,0.));
#5153=DIRECTION('ref_axis',(0.,0.,-1.));
#5154=DIRECTION('center_axis',(1.,0.,0.));
#5155=DIRECTION('ref_axis',(0.,0.,-1.));
#5156=DIRECTION('',(1.,0.,0.));
#5157=DIRECTION('center_axis',(-1.,0.,0.));
#5158=DIRECTION('ref_axis',(0.,0.,-1.));
#5159=DIRECTION('center_axis',(1.,0.,0.));
#5160=DIRECTION('ref_axis',(0.,0.,-1.));
#5161=DIRECTION('center_axis',(1.,0.,0.));
#5162=DIRECTION('ref_axis',(0.,0.,-1.));
#5163=DIRECTION('center_axis',(1.,0.,0.));
#5164=DIRECTION('ref_axis',(0.,0.,-1.));
#5165=DIRECTION('center_axis',(1.,0.,0.));
#5166=DIRECTION('ref_axis',(0.,0.,-1.));
#5167=DIRECTION('',(-1.,0.,0.));
#5168=DIRECTION('center_axis',(1.,0.,0.));
#5169=DIRECTION('ref_axis',(0.,0.,-1.));
#5170=DIRECTION('center_axis',(1.,0.,0.));
#5171=DIRECTION('ref_axis',(0.,0.,-1.));
#5172=DIRECTION('center_axis',(-1.,0.,0.));
#5173=DIRECTION('ref_axis',(0.,0.,-1.));
#5174=DIRECTION('',(-1.,0.,0.));
#5175=DIRECTION('center_axis',(-1.,0.,0.));
#5176=DIRECTION('ref_axis',(0.,0.,-1.));
#5177=DIRECTION('center_axis',(1.,0.,0.));
#5178=DIRECTION('ref_axis',(0.,0.,-1.));
#5179=DIRECTION('center_axis',(1.,0.,0.));
#5180=DIRECTION('ref_axis',(0.,0.,-1.));
#5181=DIRECTION('',(-1.,0.,0.));
#5182=DIRECTION('center_axis',(1.,0.,0.));
#5183=DIRECTION('ref_axis',(0.,0.,-1.));
#5184=DIRECTION('center_axis',(1.,0.,0.));
#5185=DIRECTION('ref_axis',(0.,0.,-1.));
#6301=CARTESIAN_POINT('',(0.,0.,0.));
#6302=CARTESIAN_POINT('Origin',(0.,-1.90918830920368,4.09081169079632));
#6303=CARTESIAN_POINT('',(0.1,-1.90918830920368,4.53081169079632));
#6304=CARTESIAN_POINT('Origin',(0.1,-1.90918830920368,4.09081169079632));
#6305=CARTESIAN_POINT('',(0.8,-1.90918830920368,4.53081169079632));
#6306=CARTESIAN_POINT('',(0.,-1.90918830920368,4.53081169079632));
#6307=CARTESIAN_POINT('Origin',(0.8,-1.90918830920368,4.09081169079632));
#6308=CARTESIAN_POINT('Origin',(0.,-1.90918830920368,7.90918830920368));
#6309=CARTESIAN_POINT('',(0.1,-1.90918830920368,8.34918830920368));
#6310=CARTESIAN_POINT('Origin',(0.1,-1.90918830920368,7.90918830920368));
#6311=CARTESIAN_POINT('',(0.8,-1.90918830920368,8.34918830920368));
#6312=CARTESIAN_POINT('',(0.,-1.90918830920368,8.34918830920368));
#6313=CARTESIAN_POINT('Origin',(0.8,-1.90918830920368,7.90918830920368));
#6314=CARTESIAN_POINT('Origin',(0.,1.90918830920368,7.90918830920368));
#6315=CARTESIAN_POINT('',(0.1,1.90918830920368,8.34918830920368));
#6316=CARTESIAN_POINT('Origin',(0.1,1.90918830920368,7.90918830920368));
#6317=CARTESIAN_POINT('',(0.8,1.90918830920368,8.34918830920368));
#6318=CARTESIAN_POINT('',(0.,1.90918830920368,8.34918830920368));
#6319=CARTESIAN_POINT('Origin',(0.8,1.90918830920368,7.90918830920368));
#6320=CARTESIAN_POINT('Origin',(0.,1.90918830920368,4.09081169079632));
#6321=CARTESIAN_POINT('',(0.1,1.90918830920368,4.53081169079632));
#6322=CARTESIAN_POINT('Origin',(0.1,1.90918830920368,4.09081169079632));
#6323=CARTESIAN_POINT('',(0.8,1.90918830920368,4.53081169079632));
#6324=CARTESIAN_POINT('',(0.,1.90918830920368,4.53081169079632));
#6325=CARTESIAN_POINT('Origin',(0.8,1.90918830920368,4.09081169079632));
#6326=CARTESIAN_POINT('Origin',(0.8,0.,6.));
#6327=CARTESIAN_POINT('',(0.8,-4.28626379701574E-16,9.5));
#6328=CARTESIAN_POINT('Origin',(0.8,0.,6.));
#6329=CARTESIAN_POINT('',(0.8,-1.83697019872103E-16,7.5));
#6330=CARTESIAN_POINT('Origin',(0.8,0.,6.));
#6331=CARTESIAN_POINT('Origin',(0.1,0.,6.));
#6332=CARTESIAN_POINT('',(0.1,-4.28626379701574E-16,9.5));
#6333=CARTESIAN_POINT('',(0.1,-4.28626379701574E-16,9.5));
#6334=CARTESIAN_POINT('Origin',(0.1,0.,6.));
#6335=CARTESIAN_POINT('Origin',(0.1,0.,6.));
#6336=CARTESIAN_POINT('',(2.8,-9.67470971326409E-17,6.79));
#6337=CARTESIAN_POINT('Origin',(2.8,0.,6.));
#6338=CARTESIAN_POINT('',(0.1,-9.67470971326409E-17,6.79));
#6339=CARTESIAN_POINT('',(0.1,-9.67470971326409E-17,6.79));
#6340=CARTESIAN_POINT('Origin',(0.1,0.,6.));
#6341=CARTESIAN_POINT('Origin',(0.1,0.,6.));
#6342=CARTESIAN_POINT('',(2.8,-1.83697019872103E-16,7.5));
#6343=CARTESIAN_POINT('Origin',(2.8,0.,6.));
#6344=CARTESIAN_POINT('',(0.1,-1.83697019872103E-16,7.5));
#6345=CARTESIAN_POINT('Origin',(2.8,0.,6.));
#6346=CARTESIAN_POINT('Origin',(0.1,0.,6.));
#6848=UNCERTAINTY_MEASURE_WITH_UNIT(LENGTH_MEASURE(0.001),#6879,
'DISTANCE_ACCURACY_VALUE',
'Maximum model space distance between geometric entities at asserted c
onnectivities');
#6857=UNCERTAINTY_MEASURE_WITH_UNIT(LENGTH_MEASURE(0.001),#6879,
'DISTANCE_ACCURACY_VALUE',
'Maximum model space distance between geometric entities at asserted c
onnectivities');
#6869=(
GEOMETRIC_REPRESENTATION_CONTEXT(3)
GLOBAL_UNCERTAINTY_ASSIGNED_CONTEXT((#6848))
GLOBAL_UNIT_ASSIGNED_CONTEXT((#6879,#6881,#6882))
REPRESENTATION_CONTEXT('','3D')
);
#6878=(
GEOMETRIC_REPRESENTATION_CONTEXT(3)
GLOBAL_UNCERTAINTY_ASSIGNED_CONTEXT((#6857))
GLOBAL_UNIT_ASSIGNED_CONTEXT((#6879,#6881,#6882))
REPRESENTATION_CONTEXT('','3D')
);
#6879=(
LENGTH_UNIT()
NAMED_UNIT(*)
SI_UNIT(.CENTI.,.METRE.)
);
#6881=(
NAMED_UNIT(*)
PLANE_ANGLE_UNIT()
SI_UNIT($,.RADIAN.)
);
#6882=(
NAMED_UNIT(*)
SI_UNIT($,.STERADIAN.)
SOLID_ANGLE_UNIT()
);
#6894=SHAPE_DEFINITION_REPRESENTATION(#6914,#6974);
#6914=PRODUCT_DEFINITION_SHAPE('',$,#6995);
#6974=SHAPE_REPRESENTATION('',(#4295),#6869);
#6983=PRODUCT_DEFINITION_CONTEXT('part definition',#7045,'design');
#6995=PRODUCT_DEFINITION('Union half B','Union half B',#7015,
#6983);
#7015=PRODUCT_DEFINITION_FORMATION('',$,#7058);
#7045=APPLICATION_CONTEXT(
'Core Data for Automotive Mechanical Design Process');
#7046=PRODUCT_CONTEXT('part definition',#7045,'mechanical');
#7058=PRODUCT('Union half B','Union half B','Union half B',
(#7046));
#7116=COLOUR_RGB('Sky Blue',0.24,0.69,0.87);
#7117=FILL_AREA_STYLE_COLOUR('',#7116);
#7118=FILL_AREA_STYLE('',(#7117));
#7119=SURFACE_STYLE_FILL_AREA(#7118);
#7120=SURFACE_SIDE_STYLE('',(#7119));
#7121=SURFACE_STYLE_USAGE(.BOTH.,#7120);
#7122=PRESENTATION_STYLE_ASSIGNMENT((#7121));
ENDSEC;
END-ISO-10303-21;
